ISO-10303-21;
HEADER;
FILE_DESCRIPTION (('STEP AP214'),
    '1' );
FILE_NAME ('Indexable Carbide Insert.step',
    '2026-10-09T18:50:44',
    ( '' ),
    ( '' ),
    'SwSTEP 2.0',
    'SolidWorks 2026',
    '' );
FILE_SCHEMA (( 'AUTOMOTIVE_DESIGN' ));
ENDSEC;

DATA;
#36=VERTEX_POINT ( 'NONE', #13398 ) ;
#44=CARTESIAN_POINT ( 'NONE',  ( -15.49969986081100615, -101.3912783891275069, -6.049618808461761255 ) ) ;
#69=CARTESIAN_POINT ( 'NONE',  ( -18.09969986081100402, -102.4362639876081289, -6.675878016713550522 ) ) ;
#103=DIRECTION ( 'NONE',  ( -0.9320450512859426162, -0.3618458327180910095, 0.01896353653557692268 ) ) ;
#107=APPLICATION_CONTEXT ( 'automotive_design' ) ;
#136=EDGE_CURVE ( 'NONE', #14079, #280, #5835, .T. ) ;
#168=FACE_BOUND ( 'NONE', #682, .T. ) ;
#190=DIRECTION ( 'NONE',  ( 1.000000000000000000, 1.000000000000000078E-15, 1.000000000000000078E-15 ) ) ;
#238=ORIENTED_EDGE ( 'NONE', *, *, #5431, .T. ) ;
#246=DIRECTION ( 'NONE',  ( 0.6626200482157384997, -0.03919731383111437623, -0.7479293030032968526 ) ) ;
#276=VERTEX_POINT ( 'NONE', #1064 ) ;
#277=ORIENTED_EDGE ( 'NONE', *, *, #6216, .F. ) ;
#280=VERTEX_POINT ( 'NONE', #11617 ) ;
#304=CARTESIAN_POINT ( 'NONE',  ( -15.49969986081100437, -101.4268716156739600, -6.728778029351857981 ) ) ;
#380=PRESENTATION_STYLE_ASSIGNMENT (( #3958 ) ) ;
#406=ADVANCED_FACE ( 'NONE', ( #6600 ), #11286, .T. ) ;
#412=ORIENTED_EDGE ( 'NONE', *, *, #3457, .F. ) ;
#470=VERTEX_POINT ( 'NONE', #44 ) ;
#479=CARTESIAN_POINT ( 'NONE',  ( -18.09969986081100046, -107.0941666664711676, -4.789471339975055919 ) ) ;
#487=EDGE_LOOP ( 'NONE', ( #1278, #9865 ) ) ;
#491=DIRECTION ( 'NONE',  ( -0.1908089953765440827, -0.9802818975087835840, 0.05137439731980028568 ) ) ;
#547=CARTESIAN_POINT ( 'NONE',  ( -15.64858178355719964, -107.2459911536667505, -7.686455132697844306 ) ) ;
#666=STYLED_ITEM ( 'NONE', ( #380 ), #2648 ) ;
#680=CONICAL_SURFACE ( 'NONE', #9472, 1.769239858347549932, 0.8464846872172493430 ) ;
#682=EDGE_LOOP ( 'NONE', ( #8653, #5006 ) ) ;
#703=ORIENTED_EDGE ( 'NONE', *, *, #6588, .T. ) ;
#706=EDGE_CURVE ( 'NONE', #7812, #276, #2547, .T. ) ;
#775=VERTEX_POINT ( 'NONE', #3503 ) ;
#844=CARTESIAN_POINT ( 'NONE',  ( -15.49969986081100082, -110.0623785963297365, -0.7605796072322540402 ) ) ;
#862=VECTOR ( 'NONE', #4969, 1000.000000000000114 ) ;
#907=CARTESIAN_POINT ( 'NONE',  ( -18.09969986081099336, -109.5303206426348765, -10.29048042260499862 ) ) ;
#927=VECTOR ( 'NONE', #246, 1000.000000000000114 ) ;
#1064=CARTESIAN_POINT ( 'NONE',  ( -18.09969986081099336, -109.6731500378498794, -10.30222923886191388 ) ) ;
#1097=FACE_OUTER_BOUND ( 'NONE', #5270, .T. ) ;
#1119=AXIS2_PLACEMENT_3D ( 'NONE', #14284, #2727, #5103 ) ;
#1149=ORIENTED_EDGE ( 'NONE', *, *, #12807, .F. ) ;
#1170=ORIENTED_EDGE ( 'NONE', *, *, #706, .T. ) ;
#1184=AXIS2_PLACEMENT_3D ( 'NONE', #9205, #5615, #6752 ) ;
#1197=CARTESIAN_POINT ( 'NONE',  ( -16.90917998795210053, -109.7162603717569311, -10.64494302517029212 ) ) ;
#1278=ORIENTED_EDGE ( 'NONE', *, *, #13298, .T. ) ;
#1302=PRODUCT_DEFINITION_CONTEXT ( 'detailed design', #107, 'design' ) ;
#1334=EDGE_CURVE ( 'NONE', #14079, #470, #10249, .T. ) ;
#1342=DIRECTION ( 'NONE',  ( 9.804908406240741039E-16, -0.05233595624294555548, -0.9986295347545738332 ) ) ;
#1359=ORIENTED_EDGE ( 'NONE', *, *, #6811, .T. ) ;
#1382=EDGE_LOOP ( 'NONE', ( #10001, #11400, #3067, #7270 ) ) ;
#1386=( BOUNDED_CURVE ( )  B_SPLINE_CURVE ( 3, ( #8741, #2858, #5089, #6442 ),
 .UNSPECIFIED., .F., .T. ) 
 B_SPLINE_CURVE_WITH_KNOTS ( ( 4, 4 ),
 ( 5.789511490773299407, 7.299387194767466447 ),
 .UNSPECIFIED. ) 
 CURVE ( )  GEOMETRIC_REPRESENTATION_ITEM ( )  RATIONAL_B_SPLINE_CURVE ( ( 1.000000000000000000, 0.8188760873989396893, 0.8188760873989396893, 1.000000000000000000 ) ) 
 REPRESENTATION_ITEM ( '' )  );
#1506=LINE ( 'NONE', #13300, #2350 ) ;
#1597=EDGE_LOOP ( 'NONE', ( #8667, #7626, #13250, #7951 ) ) ;
#1622=AXIS2_PLACEMENT_3D ( 'NONE', #12860, #14073, #5730 ) ;
#1635=DIRECTION ( 'NONE',  ( 0.9320450512859435044, -0.1973458207444490908, -0.3038859151196102726 ) ) ;
#1705=LINE ( 'NONE', #11193, #12472 ) ;
#1709=CYLINDRICAL_SURFACE ( 'NONE', #9094, 0.4000000000000002998 ) ;
#1815=VERTEX_POINT ( 'NONE', #9845 ) ;
#1821=AXIS2_PLACEMENT_3D ( 'NONE', #2282, #9459, #3277 ) ;
#1937=CARTESIAN_POINT ( 'NONE',  ( -16.02866194833901403, -110.0647956111179866, -10.55728977053499129 ) ) ;
#1944=VERTEX_POINT ( 'NONE', #4257 ) ;
#1947=ORIENTED_EDGE ( 'NONE', *, *, #3648, .T. ) ;
#1979=CARTESIAN_POINT ( 'NONE',  ( -15.49969986081099016, -110.4502521595424298, -11.13806342361127832 ) ) ;
#2011=PRODUCT ( 'Indexable Carbide Insert', 'Indexable Carbide Insert', '', ( #12530 ) ) ;
#2052=DIRECTION ( 'NONE',  ( -0.1908089953765463587, 0.5346324819374547177, 0.8232618274527189195 ) ) ;
#2060=VERTEX_POINT ( 'NONE', #5917 ) ;
#2063=ORIENTED_EDGE ( 'NONE', *, *, #12396, .F. ) ;
#2119=PLANE ( 'NONE',  #11019 ) ;
#2232=ORIENTED_EDGE ( 'NONE', *, *, #6822, .T. ) ;
#2253=CARTESIAN_POINT ( 'NONE',  ( -18.09969986081099336, -110.0345591146135860, -9.886379190557276431 ) ) ;
#2282=CARTESIAN_POINT ( 'NONE',  ( -15.49969986081099904, -107.1622034095870077, -6.087689735155999315 ) ) ;
#2350=VECTOR ( 'NONE', #6228, 1000.000000000000114 ) ;
#2421=DIRECTION ( 'NONE',  ( 0.9320450512859430603, -0.1645000119736390876, 0.3228494516551893012 ) ) ;
#2440=DIRECTION ( 'NONE',  ( -1.000000000000000078E-15, 0.05233595624294315463, 0.9986295347545739443 ) ) ;
#2477=DIRECTION ( 'NONE',  ( 0.000000000000000000, -0.05233595624293968518, -0.9986295347545740553 ) ) ;
#2488=LINE ( 'NONE', #14197, #7615 ) ;
#2528=ORIENTED_EDGE ( 'NONE', *, *, #4245, .T. ) ;
#2547=( BOUNDED_CURVE ( )  B_SPLINE_CURVE ( 3, ( #13910, #907, #8161, #8003 ),
 .UNSPECIFIED., .F., .T. ) 
 B_SPLINE_CURVE_WITH_KNOTS ( ( 4, 4 ),
 ( 5.266983419591660720, 5.789511490773299407 ),
 .UNSPECIFIED. ) 
 CURVE ( )  GEOMETRIC_REPRESENTATION_ITEM ( )  RATIONAL_B_SPLINE_CURVE ( ( 1.000000000000000000, 0.9773761648077839981, 0.9773761648077839981, 1.000000000000000000 ) ) 
 REPRESENTATION_ITEM ( '' )  );
#2565=DIRECTION ( 'NONE',  ( -3.660254037844389484E-16, 0.8386705679454246054, -0.5446390350150263071 ) ) ;
#2619=ORIENTED_EDGE ( 'NONE', *, *, #14466, .F. ) ;
#2639=CARTESIAN_POINT ( 'NONE',  ( -18.09969986081100402, -104.5552117914207741, -4.597543490852678438 ) ) ;
#2648=MANIFOLD_SOLID_BREP ( 'Stock-MAS-672-1', #9007 ) ;
#2654=UNCERTAINTY_MEASURE_WITH_UNIT (LENGTH_MEASURE( 1.000000000000000082E-05 ), #9849, 'distance_accuracy_value', 'NONE');
#2663=SURFACE_STYLE_FILL_AREA ( #6088 ) ;
#2727=DIRECTION ( 'NONE',  ( 1.000000000000000000, 1.000000000000000078E-15, 1.000000000000000078E-15 ) ) ;
#2729=VERTEX_POINT ( 'NONE', #547 ) ;
#2735=CARTESIAN_POINT ( 'NONE',  ( -18.09969986081100402, -102.4006707610616900, -5.996718795823452020 ) ) ;
#2858=CARTESIAN_POINT ( 'NONE',  ( -18.09969986081099336, -109.8997432187700412, -10.29035399344921764 ) ) ;
#2897=ADVANCED_FACE ( 'NONE', ( #11772 ), #3295, .T. ) ;
#2923=CARTESIAN_POINT ( 'NONE',  ( -15.49969986081099194, -110.2236589786222538, -11.14993866902398700 ) ) ;
#2932=ADVANCED_FACE ( 'NONE', ( #12631, #10550 ), #9405, .T. ) ;
#2944=ORIENTED_EDGE ( 'NONE', *, *, #9317, .F. ) ;
#3002=DIRECTION ( 'NONE',  ( -0.9816271834476640867, 0.1905474982798658068, -0.009986171232787752899 ) ) ;
#3067=ORIENTED_EDGE ( 'NONE', *, *, #8714, .F. ) ;
#3155=( NAMED_UNIT ( * ) PLANE_ANGLE_UNIT ( ) SI_UNIT ( $, .RADIAN. ) );
#3213=( BOUNDED_CURVE ( )  B_SPLINE_CURVE ( 3, ( #2923, #6425, #11106, #5072 ),
 .UNSPECIFIED., .F., .T. ) 
 B_SPLINE_CURVE_WITH_KNOTS ( ( 4, 4 ),
 ( 0.4936738164062529632, 1.016201887587897090 ),
 .UNSPECIFIED. ) 
 CURVE ( )  GEOMETRIC_REPRESENTATION_ITEM ( )  RATIONAL_B_SPLINE_CURVE ( ( 1.000000000000000000, 0.9773761648077835540, 0.9773761648077835540, 1.000000000000000000 ) ) 
 REPRESENTATION_ITEM ( '' )  );
#3228=CARTESIAN_POINT ( 'NONE',  ( -18.09969986081100402, -109.3083623989904538, -1.510811394685556808 ) ) ;
#3244=ORIENTED_EDGE ( 'NONE', *, *, #3494, .T. ) ;
#3277=DIRECTION ( 'NONE',  ( 9.804908406240741039E-16, -0.05233595624294555548, -0.9986295347545738332 ) ) ;
#3295=CYLINDRICAL_SURFACE ( 'NONE', #12129, 0.4000000000000018541 ) ;
#3379=VERTEX_POINT ( 'NONE', #8232 ) ;
#3397=CARTESIAN_POINT ( 'NONE',  ( -18.09969986081100046, -107.1622034095870077, -6.087689735156001980 ) ) ;
#3457=EDGE_CURVE ( 'NONE', #2729, #2060, #7700, .T. ) ;
#3484=EDGE_LOOP ( 'NONE', ( #8028, #12864, #10850, #4126 ) ) ;
#3494=EDGE_CURVE ( 'NONE', #2060, #775, #1506, .T. ) ;
#3503=CARTESIAN_POINT ( 'NONE',  ( -15.49969986081100082, -107.0696085497772430, -4.320874558545138022 ) ) ;
#3585=CARTESIAN_POINT ( 'NONE',  ( -17.71337442941458207, -109.6899368550501919, -1.875748381208218740 ) ) ;
#3613=VECTOR ( 'NONE', #14283, 1000.000000000000114 ) ;
#3648=EDGE_CURVE ( 'NONE', #14829, #14409, #12097, .T. ) ;
#3703=DIRECTION ( 'NONE',  ( 0.000000000000000000, -0.05233595624294329340, -0.9986295347545738332 ) ) ;
#3739=CARTESIAN_POINT ( 'NONE',  ( -15.49969986081100615, -101.3912783891275069, -6.049618808461761255 ) ) ;
#3951=ORIENTED_EDGE ( 'NONE', *, *, #6046, .T. ) ;
#3958=SURFACE_STYLE_USAGE ( .BOTH. , #9543 ) ;
#3998=LINE ( 'NONE', #8030, #11039 ) ;
#4119=( GEOMETRIC_REPRESENTATION_CONTEXT ( 3 ) GLOBAL_UNCERTAINTY_ASSIGNED_CONTEXT ( ( #8331 ) ) GLOBAL_UNIT_ASSIGNED_CONTEXT ( ( #13863, #3155, #14859 ) ) REPRESENTATION_CONTEXT ( 'NONE', 'WORKASPACE' ) );
#4121=CARTESIAN_POINT ( 'NONE',  ( -15.49969986081100437, -103.1269401686548690, -4.922466869613988827 ) ) ;
#4126=ORIENTED_EDGE ( 'NONE', *, *, #5431, .F. ) ;
#4245=EDGE_CURVE ( 'NONE', #2060, #2729, #11302, .T. ) ;
#4251=VECTOR ( 'NONE', #9297, 1000.000000000000000 ) ;
#4257=CARTESIAN_POINT ( 'NONE',  ( -15.49969986081099016, -110.5850680553859746, -10.73408862071934067 ) ) ;
#4265=CIRCLE ( 'NONE', #12825, 1.300000000000000488 ) ;
#4270=CARTESIAN_POINT ( 'NONE',  ( -18.09969986081100046, -107.1622034095870077, -6.087689735156001980 ) ) ;
#4381=CARTESIAN_POINT ( 'NONE',  ( 0.000000000000000000, 0.000000000000000000, 0.000000000000000000 ) ) ;
#4419=DIRECTION ( 'NONE',  ( -0.9320450512859425052, -0.3618458327180908984, 0.01896353653557666941 ) ) ;
#4423=( BOUNDED_CURVE ( )  B_SPLINE_CURVE ( 3, ( #10075, #8854, #1979, #11083 ),
 .UNSPECIFIED., .F., .T. ) 
 B_SPLINE_CURVE_WITH_KNOTS ( ( 4, 4 ),
 ( 5.266983419591681148, 6.776859123585839306 ),
 .UNSPECIFIED. ) 
 CURVE ( )  GEOMETRIC_REPRESENTATION_ITEM ( )  RATIONAL_B_SPLINE_CURVE ( ( 1.000000000000000000, 0.8188760873989417988, 0.8188760873989417988, 1.000000000000000000 ) ) 
 REPRESENTATION_ITEM ( '' )  );
#4435=ADVANCED_FACE ( 'NONE', ( #8809 ), #8732, .T. ) ;
#4573=ORIENTED_EDGE ( 'NONE', *, *, #11880, .F. ) ;
#4689=LINE ( 'NONE', #479, #10457 ) ;
#4701=CARTESIAN_POINT ( 'NONE',  ( -15.64858178355719964, -107.1622034095870077, -6.087689735155999315 ) ) ;
#4744=DIRECTION ( 'NONE',  ( 0.9320450512859425052, 0.3618458327180909539, -0.01896353653557691574 ) ) ;
#4782=( BOUNDED_CURVE ( )  B_SPLINE_CURVE ( 3, ( #2735, #7392, #10536, #69 ),
 .UNSPECIFIED., .F., .F. ) 
 B_SPLINE_CURVE_WITH_KNOTS ( ( 4, 4 ),
 ( 5.266983419591695359, 7.299387194767472664 ),
 .UNSPECIFIED. ) 
 CURVE ( )  GEOMETRIC_REPRESENTATION_ITEM ( )  RATIONAL_B_SPLINE_CURVE ( ( 1.000000000000000000, 0.6843990470536871484, 0.6843990470536871484, 1.000000000000000000 ) ) 
 REPRESENTATION_ITEM ( '' )  );
#4789=EDGE_CURVE ( 'NONE', #1815, #14119, #3213, .T. ) ;
#4881=AXIS2_PLACEMENT_3D ( 'NONE', #7435, #491, #3002 ) ;
#4969=DIRECTION ( 'NONE',  ( -0.9320450512859430603, 0.1645000119736390876, -0.3228494516551893012 ) ) ;
#4984=DIRECTION ( 'NONE',  ( 1.000000000000000000, 9.973326722932540411E-16, 9.491043554366112247E-16 ) ) ;
#5006=ORIENTED_EDGE ( 'NONE', *, *, #13187, .F. ) ;
#5021=ORIENTED_EDGE ( 'NONE', *, *, #13298, .F. ) ;
#5072=CARTESIAN_POINT ( 'NONE',  ( -15.49969986081099194, -110.0146955301539151, -11.10449286955627102 ) ) ;
#5089=CARTESIAN_POINT ( 'NONE',  ( -18.09969986081099336, -110.0468591183650915, -10.12107724339962722 ) ) ;
#5096=VECTOR ( 'NONE', #103, 999.9999999999998863 ) ;
#5103=DIRECTION ( 'NONE',  ( 0.000000000000000000, -0.05233595624293968518, -0.9986295347545740553 ) ) ;
#5143=EDGE_CURVE ( 'NONE', #36, #14829, #4782, .T. ) ;
#5270=EDGE_LOOP ( 'NONE', ( #9967, #6390, #2528, #8370 ) ) ;
#5341=PLANE ( 'NONE',  #12325 ) ;
#5359=VECTOR ( 'NONE', #11673, 1000.000000000000000 ) ;
#5431=EDGE_CURVE ( 'NONE', #6794, #14079, #2488, .T. ) ;
#5489=DIRECTION ( 'NONE',  ( 0.000000000000000000, 0.05233595624294329340, 0.9986295347545738332 ) ) ;
#5493=AXIS2_PLACEMENT_3D ( 'NONE', #11763, #9470, #6092 ) ;
#5565=ORIENTED_EDGE ( 'NONE', *, *, #14451, .T. ) ;
#5615=DIRECTION ( 'NONE',  ( 0.9320450512859429493, -0.1645000119736390598, 0.3228494516551898008 ) ) ;
#5660=ORIENTED_EDGE ( 'NONE', *, *, #14451, .F. ) ;
#5661=DIRECTION ( 'NONE',  ( 0.9320450512859435044, -0.1973458207444490631, -0.3038859151196097730 ) ) ;
#5664=VERTEX_POINT ( 'NONE', #6823 ) ;
#5671=ADVANCED_FACE ( 'NONE', ( #1097 ), #13730, .F. ) ;
#5730=DIRECTION ( 'NONE',  ( 9.999999999999998805E-16, -0.05233595624294299503, -0.9986295347545739443 ) ) ;
#5752=( BOUNDED_CURVE ( )  B_SPLINE_CURVE ( 3, ( #12719, #10099, #3228, #14927 ),
 .UNSPECIFIED., .F., .T. ) 
 B_SPLINE_CURVE_WITH_KNOTS ( ( 4, 4 ),
 ( 5.266983419591705129, 7.299387194767472664 ),
 .UNSPECIFIED. ) 
 CURVE ( )  GEOMETRIC_REPRESENTATION_ITEM ( )  RATIONAL_B_SPLINE_CURVE ( ( 1.000000000000000000, 0.6843990470536898130, 0.6843990470536898130, 1.000000000000000000 ) ) 
 REPRESENTATION_ITEM ( '' )  );
#5775=LINE ( 'NONE', #10449, #4251 ) ;
#5835=( BOUNDED_CURVE ( )  B_SPLINE_CURVE ( 3, ( #14763, #8011, #844, #9089 ),
 .UNSPECIFIED., .F., .T. ) 
 B_SPLINE_CURVE_WITH_KNOTS ( ( 4, 4 ),
 ( 5.266983419591685589, 7.299387194767492204 ),
 .UNSPECIFIED. ) 
 CURVE ( )  GEOMETRIC_REPRESENTATION_ITEM ( )  RATIONAL_B_SPLINE_CURVE ( ( 1.000000000000000000, 0.6843990470536787107, 0.6843990470536787107, 1.000000000000000000 ) ) 
 REPRESENTATION_ITEM ( '' )  );
#5884=CARTESIAN_POINT ( 'NONE',  ( -15.49969986081099727, -107.2547982693967583, -7.854504911766861497 ) ) ;
#5917=CARTESIAN_POINT ( 'NONE',  ( -15.64858178355719964, -107.0784156655072508, -4.488924337614155213 ) ) ;
#6046=EDGE_CURVE ( 'NONE', #3379, #6794, #5752, .T. ) ;
#6066=LINE ( 'NONE', #2639, #10698 ) ;
#6088=FILL_AREA_STYLE ('',( #14369 ) ) ;
#6092=DIRECTION ( 'NONE',  ( 9.804908406240741039E-16, -0.05233595624294555548, -0.9986295347545738332 ) ) ;
#6150=VECTOR ( 'NONE', #6262, 999.9999999999998863 ) ;
#6156=CARTESIAN_POINT ( 'NONE',  ( -18.09969986081099691, -109.8281559964656822, -5.947973080403810009 ) ) ;
#6167=( NAMED_UNIT ( * ) SI_UNIT ( $, .STERADIAN. ) SOLID_ANGLE_UNIT ( ) );
#6216=EDGE_CURVE ( 'NONE', #2729, #13889, #10718, .T. ) ;
#6228=DIRECTION ( 'NONE',  ( 0.6626200482157369454, 0.03919731383111578482, 0.7479293030032981848 ) ) ;
#6243=CARTESIAN_POINT ( 'NONE',  ( -15.49969986081100082, -109.4746705577010744, -0.8002025553967917482 ) ) ;
#6262=DIRECTION ( 'NONE',  ( 0.9320450512859426162, 0.3618458327180910095, -0.01896353653557698513 ) ) ;
#6390=ORIENTED_EDGE ( 'NONE', *, *, #6675, .T. ) ;
#6414=CARTESIAN_POINT ( 'NONE',  ( -15.49969986081099727, -107.2547982693967583, -7.854504911766861497 ) ) ;
#6423=AXIS2_PLACEMENT_3D ( 'NONE', #12668, #15028, #15103 ) ;
#6425=CARTESIAN_POINT ( 'NONE',  ( -15.49969986081099194, -110.1520963948262732, -11.15368910512049894 ) ) ;
#6429=EDGE_CURVE ( 'NONE', #7470, #3379, #9609, .T. ) ;
#6442=CARTESIAN_POINT ( 'NONE',  ( -18.09969986081099336, -110.0345591146135860, -9.886379190557276431 ) ) ;
#6491=EDGE_LOOP ( 'NONE', ( #1149, #1947, #8335, #5565 ) ) ;
#6496=LINE ( 'NONE', #7504, #14973 ) ;
#6588=EDGE_CURVE ( 'NONE', #470, #36, #11715, .T. ) ;
#6600=FACE_OUTER_BOUND ( 'NONE', #3484, .T. ) ;
#6646=AXIS2_PLACEMENT_3D ( 'NONE', #4701, #190, #2477 ) ;
#6675=EDGE_CURVE ( 'NONE', #10716, #2060, #4689, .T. ) ;
#6729=SHAPE_REPRESENTATION_RELATIONSHIP ( 'NONE' , 'NONE' ,  #10770, #9362 ) ;
#6751=FACE_OUTER_BOUND ( 'NONE', #14057, .T. ) ;
#6752=DIRECTION ( 'NONE',  ( 0.3190779711151164877, -0.04960027561187742989, -0.9464296386991939425 ) ) ;
#6766=CARTESIAN_POINT ( 'NONE',  ( -15.49969986081100437, -101.4268716156739600, -6.728778029351857981 ) ) ;
#6789=AXIS2_PLACEMENT_3D ( 'NONE', #4381, #12419, #6809 ) ;
#6794=VERTEX_POINT ( 'NONE', #10696 ) ;
#6804=ADVANCED_FACE ( 'NONE', ( #10778 ), #10627, .F. ) ;
#6809=DIRECTION ( 'NONE',  ( 1.000000000000000000, 0.000000000000000000, 0.000000000000000000 ) ) ;
#6811=EDGE_CURVE ( 'NONE', #14409, #470, #8884, .T. ) ;
#6822=EDGE_CURVE ( 'NONE', #280, #3379, #9626, .T. ) ;
#6823=CARTESIAN_POINT ( 'NONE',  ( -18.09969986081100046, -107.2302401527028337, -7.385908130336948929 ) ) ;
#7138=DIRECTION ( 'NONE',  ( 1.000000000000000000, 1.000000000000000078E-15, 1.000000000000000078E-15 ) ) ;
#7270=ORIENTED_EDGE ( 'NONE', *, *, #10466, .F. ) ;
#7370=ORIENTED_EDGE ( 'NONE', *, *, #1334, .T. ) ;
#7392=CARTESIAN_POINT ( 'NONE',  ( -18.09969986081100402, -102.1080954886104877, -6.186719399335088632 ) ) ;
#7415=VECTOR ( 'NONE', #2440, 1000.000000000000114 ) ;
#7435=CARTESIAN_POINT ( 'NONE',  ( -15.49969986081099371, -110.4767567321826078, -8.667385457847048613 ) ) ;
#7470=VERTEX_POINT ( 'NONE', #2253 ) ;
#7504=CARTESIAN_POINT ( 'NONE',  ( -15.49969986081099904, -104.4958141456593097, -8.292482351415227271 ) ) ;
#7553=ADVANCED_FACE ( 'NONE', ( #14107 ), #8552, .F. ) ;
#7615=VECTOR ( 'NONE', #2421, 1000.000000000000114 ) ;
#7626=ORIENTED_EDGE ( 'NONE', *, *, #6588, .F. ) ;
#7681=EDGE_CURVE ( 'NONE', #5664, #2729, #1705, .T. ) ;
#7700=CIRCLE ( 'NONE', #1119, 1.600959456836780204 ) ;
#7705=ORIENTED_EDGE ( 'NONE', *, *, #12807, .T. ) ;
#7734=COLOUR_RGB ( '', 0.40784314, 0.44705882, 0.49803922) ;
#7792=CIRCLE ( 'NONE', #8282, 1.769239858347549932 ) ;
#7812=VERTEX_POINT ( 'NONE', #11342 ) ;
#7837=DIRECTION ( 'NONE',  ( -1.000000000000000000, -1.000000000000000078E-15, -1.000000000000000078E-15 ) ) ;
#7848=ORIENTED_EDGE ( 'NONE', *, *, #9495, .T. ) ;
#7951=ORIENTED_EDGE ( 'NONE', *, *, #3648, .F. ) ;
#7954=ORIENTED_EDGE ( 'NONE', *, *, #9317, .T. ) ;
#8003=CARTESIAN_POINT ( 'NONE',  ( -18.09969986081099336, -109.6731500378498794, -10.30222923886191388 ) ) ;
#8011=CARTESIAN_POINT ( 'NONE',  ( -15.49969986081100082, -109.7672458301522624, -0.6102019518851511393 ) ) ;
#8028=ORIENTED_EDGE ( 'NONE', *, *, #6046, .F. ) ;
#8030=CARTESIAN_POINT ( 'NONE',  ( -16.10498554648963321, -110.4569083701214964, -10.53674001160706908 ) ) ;
#8161=CARTESIAN_POINT ( 'NONE',  ( -18.09969986081099336, -109.6015874540538846, -10.30597967495842227 ) ) ;
#8232=CARTESIAN_POINT ( 'NONE',  ( -18.09969986081100046, -109.6217528783177784, -2.009566970250350693 ) ) ;
#8257=CARTESIAN_POINT ( 'NONE',  ( -18.09969986081100402, -105.5768790231641248, -6.170773065691671277 ) ) ;
#8282=AXIS2_PLACEMENT_3D ( 'NONE', #9147, #7837, #13824 ) ;
#8289=FACE_OUTER_BOUND ( 'NONE', #15112, .T. ) ;
#8331=UNCERTAINTY_MEASURE_WITH_UNIT (LENGTH_MEASURE( 1.000000000000000082E-05 ), #13863, 'distance_accuracy_value', 'NONE');
#8335=ORIENTED_EDGE ( 'NONE', *, *, #11880, .T. ) ;
#8337=DIRECTION ( 'NONE',  ( 0.000000000000000000, 0.05233595624294329340, 0.9986295347545738332 ) ) ;
#8370=ORIENTED_EDGE ( 'NONE', *, *, #7681, .F. ) ;
#8528=ORIENTED_EDGE ( 'NONE', *, *, #14106, .F. ) ;
#8549=CARTESIAN_POINT ( 'NONE',  ( -15.49969986081100437, -101.1160386300729357, -6.570400712645788843 ) ) ;
#8552=CONICAL_SURFACE ( 'NONE', #14913, 1.300000000000000488, 0.1221730476396025861 ) ;
#8653=ORIENTED_EDGE ( 'NONE', *, *, #10478, .F. ) ;
#8667=ORIENTED_EDGE ( 'NONE', *, *, #5143, .F. ) ;
#8711=CARTESIAN_POINT ( 'NONE',  ( -16.90917998795211119, -101.9740710344159140, -6.700100522990623197 ) ) ;
#8714=EDGE_CURVE ( 'NONE', #1944, #1815, #4423, .T. ) ;
#8732=PLANE ( 'NONE',  #4881 ) ;
#8741=CARTESIAN_POINT ( 'NONE',  ( -18.09969986081099336, -109.6731500378498794, -10.30222923886191388 ) ) ;
#8809=FACE_OUTER_BOUND ( 'NONE', #10329, .T. ) ;
#8842=PRODUCT_DEFINITION_SHAPE ( 'NONE', 'NONE',  #12004 ) ;
#8854=CARTESIAN_POINT ( 'NONE',  ( -15.49969986081099016, -110.5973680591374944, -10.96878667356168791 ) ) ;
#8884=( BOUNDED_CURVE ( )  B_SPLINE_CURVE ( 3, ( #304, #8549, #10623, #3739 ),
 .UNSPECIFIED., .F., .F. ) 
 B_SPLINE_CURVE_WITH_KNOTS ( ( 4, 4 ),
 ( 5.266983419591701576, 7.299387194767476217 ),
 .UNSPECIFIED. ) 
 CURVE ( )  GEOMETRIC_REPRESENTATION_ITEM ( )  RATIONAL_B_SPLINE_CURVE ( ( 1.000000000000000000, 0.6843990470536877035, 0.6843990470536877035, 1.000000000000000000 ) ) 
 REPRESENTATION_ITEM ( '' )  );
#8936=ORIENTED_EDGE ( 'NONE', *, *, #6429, .F. ) ;
#9007=CLOSED_SHELL ( 'NONE', ( #5671, #9439, #11190, #13644, #406, #2897, #6804, #7553, #2932, #12104, #4435, #13123, #10723 ) ) ;
#9030=DIRECTION ( 'NONE',  ( -1.000000000000000000, -1.000000000000000078E-15, -1.000000000000000078E-15 ) ) ;
#9089=CARTESIAN_POINT ( 'NONE',  ( -15.49969986081100082, -110.0806363094795728, -1.108957527449961233 ) ) ;
#9094=AXIS2_PLACEMENT_3D ( 'NONE', #1937, #1635, #12345 ) ;
#9147=CARTESIAN_POINT ( 'NONE',  ( -15.49969986081099904, -107.1622034095870077, -6.087689735155999315 ) ) ;
#9205=CARTESIAN_POINT ( 'NONE',  ( -17.63705083126397355, -109.2978240960466678, -1.896298140136138288 ) ) ;
#9297=DIRECTION ( 'NONE',  ( 1.366025403784438385E-15, -0.8910065241883674547, -0.4539904997395473596 ) ) ;
#9310=CARTESIAN_POINT ( 'NONE',  ( -15.49969986081099549, -110.3328521824327737, -5.921523074084650951 ) ) ;
#9317=EDGE_CURVE ( 'NONE', #6794, #36, #6066, .T. ) ;
#9362=ADVANCED_BREP_SHAPE_REPRESENTATION ( '', ( #2648, #6789 ), #4119 ) ;
#9405=PLANE ( 'NONE',  #1622 ) ;
#9416=ORIENTED_EDGE ( 'NONE', *, *, #3457, .T. ) ;
#9439=ADVANCED_FACE ( 'NONE', ( #8289 ), #680, .F. ) ;
#9459=DIRECTION ( 'NONE',  ( -1.000000000000000000, -1.000000000000000078E-15, -1.000000000000000078E-15 ) ) ;
#9470=DIRECTION ( 'NONE',  ( 1.000000000000000000, 1.000000000000000078E-15, 1.000000000000000078E-15 ) ) ;
#9472=AXIS2_PLACEMENT_3D ( 'NONE', #12980, #7138, #1342 ) ;
#9478=APPLICATION_CONTEXT ( 'automotive_design' ) ;
#9480=ORIENTED_EDGE ( 'NONE', *, *, #136, .T. ) ;
#9489=PLANE ( 'NONE',  #9856 ) ;
#9495=EDGE_CURVE ( 'NONE', #276, #7470, #1386, .T. ) ;
#9543=SURFACE_SIDE_STYLE ('',( #2663 ) ) ;
#9609=LINE ( 'NONE', #6156, #3613 ) ;
#9626=LINE ( 'NONE', #3585, #862 ) ;
#9706=MECHANICAL_DESIGN_GEOMETRIC_PRESENTATION_REPRESENTATION('',(#666),#10187);
#9819=AXIS2_PLACEMENT_3D ( 'NONE', #11561, #9030, #8337 ) ;
#9835=CIRCLE ( 'NONE', #9819, 1.300000000000000488 ) ;
#9836=VECTOR ( 'NONE', #10857, 1000.000000000000114 ) ;
#9845=CARTESIAN_POINT ( 'NONE',  ( -15.49969986081099194, -110.2236589786222538, -11.14993866902398700 ) ) ;
#9849=( LENGTH_UNIT ( ) NAMED_UNIT ( * ) SI_UNIT ( .MILLI., .METRE. ) );
#9856=AXIS2_PLACEMENT_3D ( 'NONE', #8257, #4984, #12950 ) ;
#9865=ORIENTED_EDGE ( 'NONE', *, *, #14466, .T. ) ;
#9967=ORIENTED_EDGE ( 'NONE', *, *, #10478, .T. ) ;
#10001=ORIENTED_EDGE ( 'NONE', *, *, #9495, .F. ) ;
#10075=CARTESIAN_POINT ( 'NONE',  ( -15.49969986081099016, -110.5850680553859746, -10.73408862071934067 ) ) ;
#10099=CARTESIAN_POINT ( 'NONE',  ( -18.09969986081100402, -109.6034951651679279, -1.661189050032654269 ) ) ;
#10134=ORIENTED_EDGE ( 'NONE', *, *, #13187, .T. ) ;
#10187=( GEOMETRIC_REPRESENTATION_CONTEXT ( 3 ) GLOBAL_UNCERTAINTY_ASSIGNED_CONTEXT ( ( #2654 ) ) GLOBAL_UNIT_ASSIGNED_CONTEXT ( ( #9849, #14517, #6167 ) ) REPRESENTATION_CONTEXT ( 'NONE', 'WORKASPACE' ) );
#10249=LINE ( 'NONE', #11474, #10707 ) ;
#10296=DIRECTION ( 'NONE',  ( -0.1908089953765445546, 0.4456494155713290328, -0.8746362247725203432 ) ) ;
#10304=AXIS2_PLACEMENT_3D ( 'NONE', #3397, #11501, #12737 ) ;
#10329=EDGE_LOOP ( 'NONE', ( #11491, #2232, #8936, #11576 ) ) ;
#10358=CARTESIAN_POINT ( 'NONE',  ( -18.09969986081100402, -102.4362639876081289, -6.675878016713550522 ) ) ;
#10449=CARTESIAN_POINT ( 'NONE',  ( -18.09969986081100046, -104.7252558612402140, -7.842177630015021883 ) ) ;
#10457=VECTOR ( 'NONE', #13259, 1000.000000000000114 ) ;
#10466=EDGE_CURVE ( 'NONE', #7470, #1944, #3998, .T. ) ;
#10478=EDGE_CURVE ( 'NONE', #5664, #10716, #9835, .T. ) ;
#10536=CARTESIAN_POINT ( 'NONE',  ( -18.09969986081100402, -102.1254310020070761, -6.517500700007478720 ) ) ;
#10550=FACE_BOUND ( 'NONE', #487, .T. ) ;
#10556=EDGE_LOOP ( 'NONE', ( #11296, #10134, #11258, #9416 ) ) ;
#10623=CARTESIAN_POINT ( 'NONE',  ( -15.49969986081100437, -101.0987031166763188, -6.239619411973396090 ) ) ;
#10627=CONICAL_SURFACE ( 'NONE', #5493, 1.769239858347549932, 0.8464846872172493430 ) ;
#10696=CARTESIAN_POINT ( 'NONE',  ( -18.09969986081100402, -109.0157871265392799, -1.700811998197179431 ) ) ;
#10698=VECTOR ( 'NONE', #2565, 1000.000000000000000 ) ;
#10707=VECTOR ( 'NONE', #14414, 1000.000000000000000 ) ;
#10716=VERTEX_POINT ( 'NONE', #12606 ) ;
#10718=LINE ( 'NONE', #5884, #927 ) ;
#10723=ADVANCED_FACE ( 'NONE', ( #11447 ), #2119, .T. ) ;
#10770=SHAPE_REPRESENTATION ( 'Indexable Carbide Insert', ( #6789 ), #4119 ) ;
#10778=FACE_OUTER_BOUND ( 'NONE', #14853, .T. ) ;
#10850=ORIENTED_EDGE ( 'NONE', *, *, #136, .F. ) ;
#10857=DIRECTION ( 'NONE',  ( 0.9320450512859433934, -0.1973458207444490908, -0.3038859151196102171 ) ) ;
#10865=CIRCLE ( 'NONE', #1821, 1.769239858347549932 ) ;
#11019=AXIS2_PLACEMENT_3D ( 'NONE', #12524, #10296, #4419 ) ;
#11039=VECTOR ( 'NONE', #5661, 1000.000000000000000 ) ;
#11083=CARTESIAN_POINT ( 'NONE',  ( -15.49969986081099194, -110.2236589786222538, -11.14993866902398700 ) ) ;
#11106=CARTESIAN_POINT ( 'NONE',  ( -15.49969986081099194, -110.0808295834072652, -11.13818985276707707 ) ) ;
#11128=ORIENTED_EDGE ( 'NONE', *, *, #6429, .T. ) ;
#11190=ADVANCED_FACE ( 'NONE', ( #12194 ), #1709, .T. ) ;
#11193=CARTESIAN_POINT ( 'NONE',  ( -18.09969986081100046, -107.2302401527028337, -7.385908130336948929 ) ) ;
#11258=ORIENTED_EDGE ( 'NONE', *, *, #7681, .T. ) ;
#11286=CYLINDRICAL_SURFACE ( 'NONE', #1184, 0.3999999999999998557 ) ;
#11296=ORIENTED_EDGE ( 'NONE', *, *, #6675, .F. ) ;
#11302=CIRCLE ( 'NONE', #6646, 1.600959456836780204 ) ;
#11306=DIRECTION ( 'NONE',  ( -1.000000000000000000, -1.000000000000000078E-15, -1.000000000000000078E-15 ) ) ;
#11307=ORIENTED_EDGE ( 'NONE', *, *, #706, .F. ) ;
#11342=CARTESIAN_POINT ( 'NONE',  ( -18.09969986081099336, -109.4641865893815407, -10.25678343939419968 ) ) ;
#11400=ORIENTED_EDGE ( 'NONE', *, *, #14106, .T. ) ;
#11447=FACE_OUTER_BOUND ( 'NONE', #6491, .T. ) ;
#11474=CARTESIAN_POINT ( 'NONE',  ( -15.49969986081100437, -104.2799573210345869, -4.173688775771633885 ) ) ;
#11491=ORIENTED_EDGE ( 'NONE', *, *, #12396, .T. ) ;
#11501=DIRECTION ( 'NONE',  ( 1.000000000000000000, 1.000000000000000078E-15, 1.000000000000000078E-15 ) ) ;
#11561=CARTESIAN_POINT ( 'NONE',  ( -18.09969986081100046, -107.1622034095870077, -6.087689735156001980 ) ) ;
#11576=ORIENTED_EDGE ( 'NONE', *, *, #10466, .T. ) ;
#11617=CARTESIAN_POINT ( 'NONE',  ( -15.49969986081100082, -110.0806363094795728, -1.108957527449961233 ) ) ;
#11620=CARTESIAN_POINT ( 'NONE',  ( -16.83285638980149201, -102.1523308006444353, -6.350246033081615948 ) ) ;
#11673=DIRECTION ( 'NONE',  ( -0.9320450512859435044, 0.1973458207444490631, 0.3038859151196097730 ) ) ;
#11715=LINE ( 'NONE', #13035, #5096 ) ;
#11728=DIRECTION ( 'NONE',  ( 1.000000000000000000, 1.000000000000000078E-15, 1.000000000000000078E-15 ) ) ;
#11733=CYLINDRICAL_SURFACE ( 'NONE', #6423, 0.4000000000000002998 ) ;
#11759=EDGE_LOOP ( 'NONE', ( #7370, #703, #2944, #238 ) ) ;
#11763=CARTESIAN_POINT ( 'NONE',  ( -15.49969986081099904, -107.1622034095870077, -6.087689735155999315 ) ) ;
#11772=FACE_OUTER_BOUND ( 'NONE', #1597, .T. ) ;
#11848=LINE ( 'NONE', #13312, #9836 ) ;
#11880=EDGE_CURVE ( 'NONE', #14409, #14119, #6496, .T. ) ;
#11941=FACE_OUTER_BOUND ( 'NONE', #13524, .T. ) ;
#12004=PRODUCT_DEFINITION ( 'UNKNOWN', '', #12940, #1302 ) ;
#12097=LINE ( 'NONE', #8711, #6150 ) ;
#12104=ADVANCED_FACE ( 'NONE', ( #11941, #168 ), #9489, .F. ) ;
#12129=AXIS2_PLACEMENT_3D ( 'NONE', #11620, #4744, #12942 ) ;
#12194=FACE_OUTER_BOUND ( 'NONE', #1382, .T. ) ;
#12325=AXIS2_PLACEMENT_3D ( 'NONE', #4121, #2052, #12381 ) ;
#12332=DIRECTION ( 'NONE',  ( 1.366025403784438385E-15, -0.8910065241883674547, -0.4539904997395473596 ) ) ;
#12345=DIRECTION ( 'NONE',  ( -0.3190779711151160991, -0.04960027561187737438, -0.9464296386991939425 ) ) ;
#12381=DIRECTION ( 'NONE',  ( 0.9757243316563982694, 0.01146169732403566101, 0.2187022133132789925 ) ) ;
#12396=EDGE_CURVE ( 'NONE', #1944, #280, #14294, .T. ) ;
#12419=DIRECTION ( 'NONE',  ( 0.000000000000000000, 0.000000000000000000, 1.000000000000000000 ) ) ;
#12461=FACE_OUTER_BOUND ( 'NONE', #11759, .T. ) ;
#12472=VECTOR ( 'NONE', #14709, 1000.000000000000114 ) ;
#12524=CARTESIAN_POINT ( 'NONE',  ( -15.49969986081099727, -105.7207835729139305, -8.916635449454062723 ) ) ;
#12530=PRODUCT_CONTEXT ( 'NONE', #9478, 'mechanical' ) ;
#12606=CARTESIAN_POINT ( 'NONE',  ( -18.09969986081100046, -107.0941666664711676, -4.789471339975055919 ) ) ;
#12631=FACE_OUTER_BOUND ( 'NONE', #13929, .T. ) ;
#12668=CARTESIAN_POINT ( 'NONE',  ( -16.02866194833901403, -110.0647956111179866, -10.55728977053499129 ) ) ;
#12719=CARTESIAN_POINT ( 'NONE',  ( -18.09969986081100046, -109.6217528783177784, -2.009566970250350693 ) ) ;
#12737=DIRECTION ( 'NONE',  ( 0.000000000000000000, -0.05233595624294329340, -0.9986295347545738332 ) ) ;
#12798=ORIENTED_EDGE ( 'NONE', *, *, #6216, .T. ) ;
#12807=EDGE_CURVE ( 'NONE', #14829, #7812, #5775, .T. ) ;
#12825=AXIS2_PLACEMENT_3D ( 'NONE', #4270, #11306, #5489 ) ;
#12860=CARTESIAN_POINT ( 'NONE',  ( -15.49969986081100082, -105.5768790231641105, -6.170773065691668613 ) ) ;
#12864=ORIENTED_EDGE ( 'NONE', *, *, #6822, .F. ) ;
#12940=PRODUCT_DEFINITION_FORMATION_WITH_SPECIFIED_SOURCE ( 'ANY', '', #2011, .NOT_KNOWN. ) ;
#12942=DIRECTION ( 'NONE',  ( 0.3623424103984807521, -0.9307677159359857288, 0.04877946902055359940 ) ) ;
#12950=DIRECTION ( 'NONE',  ( 9.999999999999998805E-16, -0.05233595624294299503, -0.9986295347545739443 ) ) ;
#12980=CARTESIAN_POINT ( 'NONE',  ( -15.49969986081099904, -107.1622034095870077, -6.087689735155999315 ) ) ;
#13035=CARTESIAN_POINT ( 'NONE',  ( -16.10498554648964387, -101.6262671406525016, -6.037303569837844108 ) ) ;
#13049=CARTESIAN_POINT ( 'NONE',  ( -18.09969986081100046, -107.1622034095870077, -6.087689735156001980 ) ) ;
#13123=ADVANCED_FACE ( 'NONE', ( #12461 ), #5341, .T. ) ;
#13176=ORIENTED_EDGE ( 'NONE', *, *, #4789, .F. ) ;
#13187=EDGE_CURVE ( 'NONE', #10716, #5664, #4265, .T. ) ;
#13250=ORIENTED_EDGE ( 'NONE', *, *, #6811, .F. ) ;
#13259=DIRECTION ( 'NONE',  ( 0.9925461516413219831, 0.006378148623808976847, 0.1217023257055283719 ) ) ;
#13298=EDGE_CURVE ( 'NONE', #13889, #775, #10865, .T. ) ;
#13300=CARTESIAN_POINT ( 'NONE',  ( -15.49969986081100082, -107.0696085497772430, -4.320874558545138022 ) ) ;
#13312=CARTESIAN_POINT ( 'NONE',  ( -16.15629313678505952, -110.0846357213627300, -10.93586162601466860 ) ) ;
#13398=CARTESIAN_POINT ( 'NONE',  ( -18.09969986081100402, -102.4006707610616900, -5.996718795823452020 ) ) ;
#13524=EDGE_LOOP ( 'NONE', ( #7954, #14049, #7705, #1170, #7848, #11128, #3951 ) ) ;
#13565=ORIENTED_EDGE ( 'NONE', *, *, #3494, .F. ) ;
#13615=ORIENTED_EDGE ( 'NONE', *, *, #4789, .T. ) ;
#13644=ADVANCED_FACE ( 'NONE', ( #6751 ), #11733, .T. ) ;
#13730=CONICAL_SURFACE ( 'NONE', #10304, 1.300000000000000488, 0.1221730476396025861 ) ;
#13824=DIRECTION ( 'NONE',  ( 9.804908406240741039E-16, -0.05233595624294555548, -0.9986295347545738332 ) ) ;
#13863=( LENGTH_UNIT ( ) NAMED_UNIT ( * ) SI_UNIT ( .MILLI., .METRE. ) );
#13889=VERTEX_POINT ( 'NONE', #6414 ) ;
#13910=CARTESIAN_POINT ( 'NONE',  ( -18.09969986081099336, -109.4641865893815407, -10.25678343939419968 ) ) ;
#13929=EDGE_LOOP ( 'NONE', ( #4573, #1359, #14328, #9480, #2063, #13933, #13615 ) ) ;
#13933=ORIENTED_EDGE ( 'NONE', *, *, #8714, .T. ) ;
#14049=ORIENTED_EDGE ( 'NONE', *, *, #5143, .T. ) ;
#14057=EDGE_LOOP ( 'NONE', ( #8528, #11307, #5660, #13176 ) ) ;
#14073=DIRECTION ( 'NONE',  ( 1.000000000000000000, 9.973326722932540411E-16, 9.491043554366112247E-16 ) ) ;
#14079=VERTEX_POINT ( 'NONE', #6243 ) ;
#14106=EDGE_CURVE ( 'NONE', #276, #1815, #11848, .T. ) ;
#14107=FACE_OUTER_BOUND ( 'NONE', #10556, .T. ) ;
#14119=VERTEX_POINT ( 'NONE', #14222 ) ;
#14197=CARTESIAN_POINT ( 'NONE',  ( -17.71337442941458207, -109.0839711032716934, -1.566993409155049255 ) ) ;
#14222=CARTESIAN_POINT ( 'NONE',  ( -15.49969986081099194, -110.0146955301539151, -11.10449286955627102 ) ) ;
#14283=DIRECTION ( 'NONE',  ( -1.000000000000000078E-15, 0.05233595624294315463, 0.9986295347545739443 ) ) ;
#14284=CARTESIAN_POINT ( 'NONE',  ( -15.64858178355719964, -107.1622034095870077, -6.087689735155999315 ) ) ;
#14294=LINE ( 'NONE', #9310, #7415 ) ;
#14322=SHAPE_DEFINITION_REPRESENTATION ( #8842, #10770 ) ;
#14328=ORIENTED_EDGE ( 'NONE', *, *, #1334, .F. ) ;
#14369=FILL_AREA_STYLE_COLOUR ( '', #7734 ) ;
#14409=VERTEX_POINT ( 'NONE', #6766 ) ;
#14414=DIRECTION ( 'NONE',  ( -3.660254037844389484E-16, 0.8386705679454246054, -0.5446390350150263071 ) ) ;
#14451=EDGE_CURVE ( 'NONE', #14119, #7812, #14970, .T. ) ;
#14466=EDGE_CURVE ( 'NONE', #775, #13889, #7792, .T. ) ;
#14517=( NAMED_UNIT ( * ) PLANE_ANGLE_UNIT ( ) SI_UNIT ( $, .RADIAN. ) );
#14709=DIRECTION ( 'NONE',  ( 0.9925461516413222052, -0.006378148623806976711, -0.1217023257055263735 ) ) ;
#14721=ORIENTED_EDGE ( 'NONE', *, *, #4245, .F. ) ;
#14763=CARTESIAN_POINT ( 'NONE',  ( -15.49969986081100082, -109.4746705577010744, -0.8002025553967917482 ) ) ;
#14829=VERTEX_POINT ( 'NONE', #10358 ) ;
#14853=EDGE_LOOP ( 'NONE', ( #13565, #412, #12798, #2619 ) ) ;
#14859=( NAMED_UNIT ( * ) SI_UNIT ( $, .STERADIAN. ) SOLID_ANGLE_UNIT ( ) );
#14913=AXIS2_PLACEMENT_3D ( 'NONE', #13049, #11728, #3703 ) ;
#14927=CARTESIAN_POINT ( 'NONE',  ( -18.09969986081100402, -109.0157871265392799, -1.700811998197179431 ) ) ;
#14970=LINE ( 'NONE', #1197, #5359 ) ;
#14973=VECTOR ( 'NONE', #12332, 1000.000000000000000 ) ;
#15028=DIRECTION ( 'NONE',  ( 0.9320450512859435044, -0.1973458207444490908, -0.3038859151196102726 ) ) ;
#15103=DIRECTION ( 'NONE',  ( -0.3190779711151160991, -0.04960027561187737438, -0.9464296386991939425 ) ) ;
#15112=EDGE_LOOP ( 'NONE', ( #14721, #3244, #5021, #277 ) ) ;
ENDSEC;
END-ISO-10303-21;
